ISO-10303-21;
HEADER;
/* Generated by software containing ST-Developer
 * from STEP Tools, Inc. (www.steptools.com) 
 */

FILE_DESCRIPTION(
/* description */ ('Grid plate located blocks and clamp'),
/* implementation_level */ '2;1');

FILE_NAME(
/* name */ 'M4x10 Cap Screw.step',
/* time_stamp */ '2026-10-29T15:43:47-07:00',
/* author */ (''),
/* organization */ (''),
/* preprocessor_version */ 'ST-DEVELOPER v20.2',
/* originating_system */ 'Autodesk Translation Framework v15.17.0.0',
/* authorisation */ '');

FILE_SCHEMA (('AUTOMOTIVE_DESIGN { 1 0 10303 214 3 1 1 }'));
ENDSEC;

DATA;
#10=MECHANICAL_DESIGN_GEOMETRIC_PRESENTATION_REPRESENTATION('',(#175),#5702);
#128=ORIENTED_CLOSED_SHELL('',*,#3271,.F.);
#133=CONICAL_SURFACE('',#3646,0.325,0.785398163397448);
#134=CONICAL_SURFACE('',#3650,0.335,0.785398163397448);
#135=CONICAL_SURFACE('',#3654,0.21,0.463647609000806);
#139=BREP_WITH_VOIDS('Body1',#3272,(#128));
#149=SHAPE_REPRESENTATION_RELATIONSHIP('SRR','None',#5767,#161);
#161=ADVANCED_BREP_SHAPE_REPRESENTATION('',(#139),#5697);
#175=STYLED_ITEM('',(#5904),#139);
#260=FACE_BOUND('',#849,.T.);
#354=CIRCLE('',#3643,0.1954);
#355=CIRCLE('',#3645,0.3);
#356=CIRCLE('',#3647,0.35);
#357=CIRCLE('',#3649,0.35);
#358=CIRCLE('',#3651,0.32);
#359=CIRCLE('',#3653,0.22);
#360=CIRCLE('',#3655,0.1954);
#438=CYLINDRICAL_SURFACE('',#3648,0.35);
#439=CYLINDRICAL_SURFACE('',#3656,0.1954);
#584=FACE_OUTER_BOUND('',#835,.T.);
#585=FACE_OUTER_BOUND('',#836,.T.);
#586=FACE_OUTER_BOUND('',#837,.T.);
#587=FACE_OUTER_BOUND('',#838,.T.);
#588=FACE_OUTER_BOUND('',#839,.T.);
#589=FACE_OUTER_BOUND('',#840,.T.);
#590=FACE_OUTER_BOUND('',#841,.T.);
#591=FACE_OUTER_BOUND('',#842,.T.);
#592=FACE_OUTER_BOUND('',#843,.T.);
#593=FACE_OUTER_BOUND('',#844,.T.);
#594=FACE_OUTER_BOUND('',#845,.T.);
#595=FACE_OUTER_BOUND('',#846,.T.);
#596=FACE_OUTER_BOUND('',#847,.T.);
#597=FACE_OUTER_BOUND('',#848,.T.);
#598=FACE_OUTER_BOUND('',#850,.T.);
#599=FACE_OUTER_BOUND('',#851,.T.);
#835=EDGE_LOOP('',(#2722,#2723,#2724,#2725));
#836=EDGE_LOOP('',(#2726,#2727,#2728,#2729));
#837=EDGE_LOOP('',(#2730,#2731,#2732,#2733));
#838=EDGE_LOOP('',(#2734,#2735,#2736,#2737));
#839=EDGE_LOOP('',(#2738,#2739,#2740,#2741));
#840=EDGE_LOOP('',(#2742,#2743,#2744,#2745));
#841=EDGE_LOOP('',(#2746,#2747,#2748,#2749,#2750,#2751));
#842=EDGE_LOOP('',(#2752,#2753,#2754,#2755,#2756,#2757));
#843=EDGE_LOOP('',(#2758));
#844=EDGE_LOOP('',(#2759));
#845=EDGE_LOOP('',(#2760,#2761,#2762,#2763));
#846=EDGE_LOOP('',(#2764,#2765,#2766,#2767));
#847=EDGE_LOOP('',(#2768,#2769,#2770,#2771));
#848=EDGE_LOOP('',(#2772));
#849=EDGE_LOOP('',(#2773));
#850=EDGE_LOOP('',(#2774,#2775,#2776,#2777));
#851=EDGE_LOOP('',(#2778,#2779,#2780,#2781));
#1106=LINE('',#5368,#1379);
#1107=LINE('',#5370,#1380);
#1108=LINE('',#5372,#1381);
#1109=LINE('',#5373,#1382);
#1110=LINE('',#5376,#1383);
#1111=LINE('',#5378,#1384);
#1112=LINE('',#5379,#1385);
#1113=LINE('',#5382,#1386);
#1114=LINE('',#5384,#1387);
#1115=LINE('',#5385,#1388);
#1116=LINE('',#5388,#1389);
#1117=LINE('',#5390,#1390);
#1118=LINE('',#5391,#1391);
#1119=LINE('',#5394,#1392);
#1120=LINE('',#5396,#1393);
#1121=LINE('',#5397,#1394);
#1122=LINE('',#5399,#1395);
#1123=LINE('',#5400,#1396);
#1124=LINE('',#5412,#1397);
#1125=LINE('',#5416,#1398);
#1126=LINE('',#5420,#1399);
#1127=LINE('',#5427,#1400);
#1128=LINE('',#5429,#1401);
#1379=VECTOR('',#4420,1.);
#1380=VECTOR('',#4421,1.);
#1381=VECTOR('',#4422,1.);
#1382=VECTOR('',#4423,1.);
#1383=VECTOR('',#4426,1.);
#1384=VECTOR('',#4427,1.);
#1385=VECTOR('',#4428,1.);
#1386=VECTOR('',#4431,1.);
#1387=VECTOR('',#4432,1.);
#1388=VECTOR('',#4433,1.);
#1389=VECTOR('',#4436,1.);
#1390=VECTOR('',#4437,1.);
#1391=VECTOR('',#4438,1.);
#1392=VECTOR('',#4441,1.);
#1393=VECTOR('',#4442,1.);
#1394=VECTOR('',#4443,1.);
#1395=VECTOR('',#4446,1.);
#1396=VECTOR('',#4447,1.);
#1397=VECTOR('',#4464,0.325);
#1398=VECTOR('',#4469,0.35);
#1399=VECTOR('',#4474,0.335);
#1400=VECTOR('',#4483,0.21);
#1401=VECTOR('',#4486,0.2);
#1637=VERTEX_POINT('',#5366);
#1638=VERTEX_POINT('',#5367);
#1639=VERTEX_POINT('',#5369);
#1640=VERTEX_POINT('',#5371);
#1641=VERTEX_POINT('',#5375);
#1642=VERTEX_POINT('',#5377);
#1643=VERTEX_POINT('',#5381);
#1644=VERTEX_POINT('',#5383);
#1645=VERTEX_POINT('',#5387);
#1646=VERTEX_POINT('',#5389);
#1647=VERTEX_POINT('',#5393);
#1648=VERTEX_POINT('',#5395);
#1649=VERTEX_POINT('',#5404);
#1650=VERTEX_POINT('',#5407);
#1651=VERTEX_POINT('',#5410);
#1652=VERTEX_POINT('',#5414);
#1653=VERTEX_POINT('',#5418);
#1654=VERTEX_POINT('',#5422);
#1655=VERTEX_POINT('',#5425);
#2011=EDGE_CURVE('',#1637,#1638,#1106,.T.);
#2012=EDGE_CURVE('',#1638,#1639,#1107,.T.);
#2013=EDGE_CURVE('',#1639,#1640,#1108,.T.);
#2014=EDGE_CURVE('',#1637,#1640,#1109,.T.);
#2015=EDGE_CURVE('',#1638,#1641,#1110,.T.);
#2016=EDGE_CURVE('',#1641,#1642,#1111,.T.);
#2017=EDGE_CURVE('',#1642,#1639,#1112,.T.);
#2018=EDGE_CURVE('',#1641,#1643,#1113,.T.);
#2019=EDGE_CURVE('',#1643,#1644,#1114,.T.);
#2020=EDGE_CURVE('',#1644,#1642,#1115,.T.);
#2021=EDGE_CURVE('',#1643,#1645,#1116,.T.);
#2022=EDGE_CURVE('',#1645,#1646,#1117,.T.);
#2023=EDGE_CURVE('',#1646,#1644,#1118,.T.);
#2024=EDGE_CURVE('',#1645,#1647,#1119,.T.);
#2025=EDGE_CURVE('',#1647,#1648,#1120,.T.);
#2026=EDGE_CURVE('',#1648,#1646,#1121,.T.);
#2027=EDGE_CURVE('',#1647,#1637,#1122,.T.);
#2028=EDGE_CURVE('',#1640,#1648,#1123,.T.);
#2029=EDGE_CURVE('',#1649,#1649,#354,.T.);
#2030=EDGE_CURVE('',#1650,#1650,#355,.T.);
#2031=EDGE_CURVE('',#1651,#1651,#356,.T.);
#2032=EDGE_CURVE('',#1651,#1650,#1124,.T.);
#2033=EDGE_CURVE('',#1652,#1652,#357,.T.);
#2034=EDGE_CURVE('',#1652,#1651,#1125,.T.);
#2035=EDGE_CURVE('',#1653,#1653,#358,.T.);
#2036=EDGE_CURVE('',#1653,#1652,#1126,.T.);
#2037=EDGE_CURVE('',#1654,#1654,#359,.T.);
#2038=EDGE_CURVE('',#1655,#1655,#360,.F.);
#2039=EDGE_CURVE('',#1655,#1654,#1127,.T.);
#2040=EDGE_CURVE('',#1649,#1655,#1128,.T.);
#2722=ORIENTED_EDGE('',*,*,#2011,.T.);
#2723=ORIENTED_EDGE('',*,*,#2012,.T.);
#2724=ORIENTED_EDGE('',*,*,#2013,.T.);
#2725=ORIENTED_EDGE('',*,*,#2014,.F.);
#2726=ORIENTED_EDGE('',*,*,#2015,.T.);
#2727=ORIENTED_EDGE('',*,*,#2016,.T.);
#2728=ORIENTED_EDGE('',*,*,#2017,.T.);
#2729=ORIENTED_EDGE('',*,*,#2012,.F.);
#2730=ORIENTED_EDGE('',*,*,#2018,.T.);
#2731=ORIENTED_EDGE('',*,*,#2019,.T.);
#2732=ORIENTED_EDGE('',*,*,#2020,.T.);
#2733=ORIENTED_EDGE('',*,*,#2016,.F.);
#2734=ORIENTED_EDGE('',*,*,#2021,.T.);
#2735=ORIENTED_EDGE('',*,*,#2022,.T.);
#2736=ORIENTED_EDGE('',*,*,#2023,.T.);
#2737=ORIENTED_EDGE('',*,*,#2019,.F.);
#2738=ORIENTED_EDGE('',*,*,#2024,.T.);
#2739=ORIENTED_EDGE('',*,*,#2025,.T.);
#2740=ORIENTED_EDGE('',*,*,#2026,.T.);
#2741=ORIENTED_EDGE('',*,*,#2022,.F.);
#2742=ORIENTED_EDGE('',*,*,#2027,.T.);
#2743=ORIENTED_EDGE('',*,*,#2014,.T.);
#2744=ORIENTED_EDGE('',*,*,#2028,.T.);
#2745=ORIENTED_EDGE('',*,*,#2025,.F.);
#2746=ORIENTED_EDGE('',*,*,#2027,.F.);
#2747=ORIENTED_EDGE('',*,*,#2024,.F.);
#2748=ORIENTED_EDGE('',*,*,#2021,.F.);
#2749=ORIENTED_EDGE('',*,*,#2018,.F.);
#2750=ORIENTED_EDGE('',*,*,#2015,.F.);
#2751=ORIENTED_EDGE('',*,*,#2011,.F.);
#2752=ORIENTED_EDGE('',*,*,#2028,.F.);
#2753=ORIENTED_EDGE('',*,*,#2013,.F.);
#2754=ORIENTED_EDGE('',*,*,#2017,.F.);
#2755=ORIENTED_EDGE('',*,*,#2020,.F.);
#2756=ORIENTED_EDGE('',*,*,#2023,.F.);
#2757=ORIENTED_EDGE('',*,*,#2026,.F.);
#2758=ORIENTED_EDGE('',*,*,#2029,.F.);
#2759=ORIENTED_EDGE('',*,*,#2030,.F.);
#2760=ORIENTED_EDGE('',*,*,#2031,.F.);
#2761=ORIENTED_EDGE('',*,*,#2032,.T.);
#2762=ORIENTED_EDGE('',*,*,#2030,.T.);
#2763=ORIENTED_EDGE('',*,*,#2032,.F.);
#2764=ORIENTED_EDGE('',*,*,#2033,.F.);
#2765=ORIENTED_EDGE('',*,*,#2034,.T.);
#2766=ORIENTED_EDGE('',*,*,#2031,.T.);
#2767=ORIENTED_EDGE('',*,*,#2034,.F.);
#2768=ORIENTED_EDGE('',*,*,#2035,.F.);
#2769=ORIENTED_EDGE('',*,*,#2036,.T.);
#2770=ORIENTED_EDGE('',*,*,#2033,.T.);
#2771=ORIENTED_EDGE('',*,*,#2036,.F.);
#2772=ORIENTED_EDGE('',*,*,#2035,.T.);
#2773=ORIENTED_EDGE('',*,*,#2037,.F.);
#2774=ORIENTED_EDGE('',*,*,#2038,.F.);
#2775=ORIENTED_EDGE('',*,*,#2039,.T.);
#2776=ORIENTED_EDGE('',*,*,#2037,.T.);
#2777=ORIENTED_EDGE('',*,*,#2039,.F.);
#2778=ORIENTED_EDGE('',*,*,#2029,.T.);
#2779=ORIENTED_EDGE('',*,*,#2040,.T.);
#2780=ORIENTED_EDGE('',*,*,#2038,.T.);
#2781=ORIENTED_EDGE('',*,*,#2040,.F.);
#3046=PLANE('',#3634);
#3047=PLANE('',#3635);
#3048=PLANE('',#3636);
#3049=PLANE('',#3637);
#3050=PLANE('',#3638);
#3051=PLANE('',#3639);
#3052=PLANE('',#3640);
#3053=PLANE('',#3641);
#3054=PLANE('',#3642);
#3055=PLANE('',#3644);
#3056=PLANE('',#3652);
#3205=ADVANCED_FACE('',(#584),#3046,.F.);
#3206=ADVANCED_FACE('',(#585),#3047,.F.);
#3207=ADVANCED_FACE('',(#586),#3048,.F.);
#3208=ADVANCED_FACE('',(#587),#3049,.F.);
#3209=ADVANCED_FACE('',(#588),#3050,.F.);
#3210=ADVANCED_FACE('',(#589),#3051,.F.);
#3211=ADVANCED_FACE('',(#590),#3052,.F.);
#3212=ADVANCED_FACE('',(#591),#3053,.F.);
#3213=ADVANCED_FACE('',(#592),#3054,.F.);
#3214=ADVANCED_FACE('',(#593),#3055,.T.);
#3215=ADVANCED_FACE('',(#594),#133,.T.);
#3216=ADVANCED_FACE('',(#595),#438,.T.);
#3217=ADVANCED_FACE('',(#596),#134,.T.);
#3218=ADVANCED_FACE('',(#597,#260),#3056,.T.);
#3219=ADVANCED_FACE('',(#598),#135,.T.);
#3220=ADVANCED_FACE('',(#599),#439,.T.);
#3271=CLOSED_SHELL('',(#3205,#3206,#3207,#3208,#3209,#3210,#3211,#3212));
#3272=CLOSED_SHELL('',(#3213,#3214,#3215,#3216,#3217,#3218,#3219,#3220));
#3633=AXIS2_PLACEMENT_3D('',#5364,#4416,#4417);
#3634=AXIS2_PLACEMENT_3D('',#5365,#4418,#4419);
#3635=AXIS2_PLACEMENT_3D('',#5374,#4424,#4425);
#3636=AXIS2_PLACEMENT_3D('',#5380,#4429,#4430);
#3637=AXIS2_PLACEMENT_3D('',#5386,#4434,#4435);
#3638=AXIS2_PLACEMENT_3D('',#5392,#4439,#4440);
#3639=AXIS2_PLACEMENT_3D('',#5398,#4444,#4445);
#3640=AXIS2_PLACEMENT_3D('',#5401,#4448,#4449);
#3641=AXIS2_PLACEMENT_3D('',#5402,#4450,#4451);
#3642=AXIS2_PLACEMENT_3D('',#5403,#4452,#4453);
#3643=AXIS2_PLACEMENT_3D('',#5405,#4454,#4455);
#3644=AXIS2_PLACEMENT_3D('',#5406,#4456,#4457);
#3645=AXIS2_PLACEMENT_3D('',#5408,#4458,#4459);
#3646=AXIS2_PLACEMENT_3D('',#5409,#4460,#4461);
#3647=AXIS2_PLACEMENT_3D('',#5411,#4462,#4463);
#3648=AXIS2_PLACEMENT_3D('',#5413,#4465,#4466);
#3649=AXIS2_PLACEMENT_3D('',#5415,#4467,#4468);
#3650=AXIS2_PLACEMENT_3D('',#5417,#4470,#4471);
#3651=AXIS2_PLACEMENT_3D('',#5419,#4472,#4473);
#3652=AXIS2_PLACEMENT_3D('',#5421,#4475,#4476);
#3653=AXIS2_PLACEMENT_3D('',#5423,#4477,#4478);
#3654=AXIS2_PLACEMENT_3D('',#5424,#4479,#4480);
#3655=AXIS2_PLACEMENT_3D('',#5426,#4481,#4482);
#3656=AXIS2_PLACEMENT_3D('',#5428,#4484,#4485);
#4416=DIRECTION('axis',(0.,0.,1.));
#4417=DIRECTION('refdir',(1.,0.,0.));
#4418=DIRECTION('center_axis',(0.866025403784439,0.,-0.5));
#4419=DIRECTION('ref_axis',(0.5,0.,0.866025403784439));
#4420=DIRECTION('',(-0.5,0.,-0.866025403784439));
#4421=DIRECTION('',(0.,-1.,0.));
#4422=DIRECTION('',(0.5,0.,0.866025403784439));
#4423=DIRECTION('',(0.,-1.,0.));
#4424=DIRECTION('center_axis',(1.60246890531964E-16,0.,-1.));
#4425=DIRECTION('ref_axis',(1.,0.,1.60246890531964E-16));
#4426=DIRECTION('',(-1.,0.,-1.60246890531964E-16));
#4427=DIRECTION('',(0.,-1.,0.));
#4428=DIRECTION('',(1.,0.,1.60246890531964E-16));
#4429=DIRECTION('center_axis',(-0.866025403784439,0.,-0.5));
#4430=DIRECTION('ref_axis',(0.5,0.,-0.866025403784439));
#4431=DIRECTION('',(-0.5,0.,0.866025403784439));
#4432=DIRECTION('',(0.,-1.,0.));
#4433=DIRECTION('',(0.5,0.,-0.866025403784439));
#4434=DIRECTION('center_axis',(-0.866025403784439,0.,0.5));
#4435=DIRECTION('ref_axis',(-0.5,0.,-0.866025403784439));
#4436=DIRECTION('',(0.5,0.,0.866025403784439));
#4437=DIRECTION('',(0.,-1.,0.));
#4438=DIRECTION('',(-0.5,0.,-0.866025403784439));
#4439=DIRECTION('center_axis',(-1.60246890531964E-16,0.,1.));
#4440=DIRECTION('ref_axis',(-1.,0.,-1.60246890531964E-16));
#4441=DIRECTION('',(1.,0.,1.60246890531964E-16));
#4442=DIRECTION('',(0.,-1.,0.));
#4443=DIRECTION('',(-1.,0.,-1.60246890531964E-16));
#4444=DIRECTION('center_axis',(0.866025403784439,0.,0.5));
#4445=DIRECTION('ref_axis',(-0.5,0.,0.866025403784439));
#4446=DIRECTION('',(0.5,0.,-0.866025403784439));
#4447=DIRECTION('',(-0.5,0.,0.866025403784439));
#4448=DIRECTION('center_axis',(0.,1.,0.));
#4449=DIRECTION('ref_axis',(1.,0.,0.));
#4450=DIRECTION('center_axis',(0.,-1.,0.));
#4451=DIRECTION('ref_axis',(0.,0.,-1.));
#4452=DIRECTION('center_axis',(0.,1.,0.));
#4453=DIRECTION('ref_axis',(1.,0.,0.));
#4454=DIRECTION('center_axis',(0.,1.,0.));
#4455=DIRECTION('ref_axis',(1.,0.,0.));
#4456=DIRECTION('center_axis',(0.,1.,0.));
#4457=DIRECTION('ref_axis',(0.,0.,1.));
#4458=DIRECTION('center_axis',(0.,-1.,0.));
#4459=DIRECTION('ref_axis',(1.,0.,0.));
#4460=DIRECTION('center_axis',(0.,-1.,0.));
#4461=DIRECTION('ref_axis',(1.,0.,0.));
#4462=DIRECTION('center_axis',(0.,-1.,0.));
#4463=DIRECTION('ref_axis',(1.,0.,0.));
#4464=DIRECTION('',(0.707106781186547,0.707106781186548,8.65956056235493E-17));
#4465=DIRECTION('center_axis',(0.,-1.,0.));
#4466=DIRECTION('ref_axis',(1.,0.,0.));
#4467=DIRECTION('center_axis',(0.,-1.,0.));
#4468=DIRECTION('ref_axis',(1.,0.,0.));
#4469=DIRECTION('',(0.,1.,0.));
#4470=DIRECTION('center_axis',(0.,1.,0.));
#4471=DIRECTION('ref_axis',(1.,0.,0.));
#4472=DIRECTION('center_axis',(0.,-1.,0.));
#4473=DIRECTION('ref_axis',(1.,0.,0.));
#4474=DIRECTION('',(-0.707106781186547,0.707106781186548,-8.65956056235493E-17));
#4475=DIRECTION('center_axis',(0.,-1.,0.));
#4476=DIRECTION('ref_axis',(0.,0.,-1.));
#4477=DIRECTION('center_axis',(0.,-1.,0.));
#4478=DIRECTION('ref_axis',(1.,0.,0.));
#4479=DIRECTION('center_axis',(0.,1.,0.));
#4480=DIRECTION('ref_axis',(1.,0.,0.));
#4481=DIRECTION('center_axis',(0.,1.,0.));
#4482=DIRECTION('ref_axis',(1.,0.,0.));
#4483=DIRECTION('',(-0.447213595499958,0.894427190999916,-5.47678698264203E-17));
#4484=DIRECTION('center_axis',(0.,-1.,0.));
#4485=DIRECTION('ref_axis',(1.,0.,0.));
#4486=DIRECTION('',(0.,1.,0.));
#5364=CARTESIAN_POINT('',(0.,0.,0.));
#5365=CARTESIAN_POINT('Origin',(0.0866025403784439,-0.4,-0.15));
#5366=CARTESIAN_POINT('',(0.173205080756888,-0.4,0.));
#5367=CARTESIAN_POINT('',(0.0866025403784439,-0.4,-0.15));
#5368=CARTESIAN_POINT('',(0.173205080756888,-0.4,0.));
#5369=CARTESIAN_POINT('',(0.0866025403784439,-0.64,-0.15));
#5370=CARTESIAN_POINT('',(0.0866025403784439,-0.4,-0.15));
#5371=CARTESIAN_POINT('',(0.173205080756888,-0.64,0.));
#5372=CARTESIAN_POINT('',(0.173205080756888,-0.64,0.));
#5373=CARTESIAN_POINT('',(0.173205080756888,-0.4,0.));
#5374=CARTESIAN_POINT('Origin',(-0.0866025403784438,-0.4,-0.15));
#5375=CARTESIAN_POINT('',(-0.0866025403784438,-0.4,-0.15));
#5376=CARTESIAN_POINT('',(0.0866025403784439,-0.4,-0.15));
#5377=CARTESIAN_POINT('',(-0.0866025403784438,-0.64,-0.15));
#5378=CARTESIAN_POINT('',(-0.0866025403784438,-0.4,-0.15));
#5379=CARTESIAN_POINT('',(0.0866025403784439,-0.64,-0.15));
#5380=CARTESIAN_POINT('Origin',(-0.173205080756888,-0.4,-2.77555756156289E-17));
#5381=CARTESIAN_POINT('',(-0.173205080756888,-0.4,-2.12115047744981E-17));
#5382=CARTESIAN_POINT('',(-0.0866025403784438,-0.4,-0.15));
#5383=CARTESIAN_POINT('',(-0.173205080756888,-0.64,-2.77555756156289E-17));
#5384=CARTESIAN_POINT('',(-0.173205080756888,-0.4,-2.12115047744981E-17));
#5385=CARTESIAN_POINT('',(-0.0866025403784438,-0.64,-0.15));
#5386=CARTESIAN_POINT('Origin',(-0.0866025403784439,-0.4,0.15));
#5387=CARTESIAN_POINT('',(-0.0866025403784439,-0.4,0.15));
#5388=CARTESIAN_POINT('',(-0.173205080756888,-0.4,-2.12115047744981E-17));
#5389=CARTESIAN_POINT('',(-0.0866025403784439,-0.64,0.15));
#5390=CARTESIAN_POINT('',(-0.0866025403784439,-0.4,0.15));
#5391=CARTESIAN_POINT('',(-0.173205080756888,-0.64,-2.12115047744981E-17));
#5392=CARTESIAN_POINT('Origin',(0.0866025403784439,-0.4,0.15));
#5393=CARTESIAN_POINT('',(0.0866025403784439,-0.4,0.15));
#5394=CARTESIAN_POINT('',(-0.0866025403784439,-0.4,0.15));
#5395=CARTESIAN_POINT('',(0.0866025403784439,-0.64,0.15));
#5396=CARTESIAN_POINT('',(0.0866025403784439,-0.4,0.15));
#5397=CARTESIAN_POINT('',(-0.0866025403784439,-0.64,0.15));
#5398=CARTESIAN_POINT('Origin',(0.173205080756888,-0.4,0.));
#5399=CARTESIAN_POINT('',(0.0866025403784439,-0.4,0.15));
#5400=CARTESIAN_POINT('',(0.0866025403784439,-0.64,0.15));
#5401=CARTESIAN_POINT('Origin',(0.,-0.4,-2.77555756156289E-17));
#5402=CARTESIAN_POINT('Origin',(0.,-0.64,-2.77555756156289E-17));
#5403=CARTESIAN_POINT('Origin',(0.,-1.,0.));
#5404=CARTESIAN_POINT('',(-0.1954,-1.,2.39295984553393E-17));
#5405=CARTESIAN_POINT('Origin',(0.,-1.,0.));
#5406=CARTESIAN_POINT('Origin',(0.3,0.4,0.));
#5407=CARTESIAN_POINT('',(-0.3,0.4,-3.67394039744206E-17));
#5408=CARTESIAN_POINT('Origin',(0.,0.4,0.));
#5409=CARTESIAN_POINT('Origin',(0.,0.375,0.));
#5410=CARTESIAN_POINT('',(-0.35,0.35,-4.28626379701573E-17));
#5411=CARTESIAN_POINT('Origin',(0.,0.35,0.));
#5412=CARTESIAN_POINT('',(-0.325,0.375,-3.9801020972289E-17));
#5413=CARTESIAN_POINT('Origin',(0.,0.19,0.));
#5414=CARTESIAN_POINT('',(-0.35,0.03,-4.28626379701574E-17));
#5415=CARTESIAN_POINT('Origin',(0.,0.03,0.));
#5416=CARTESIAN_POINT('',(-0.35,0.19,-4.28626379701574E-17));
#5417=CARTESIAN_POINT('Origin',(0.,0.0149999999999999,0.));
#5418=CARTESIAN_POINT('',(-0.32,-3.29597460435593E-17,-3.91886975727153E-17));
#5419=CARTESIAN_POINT('Origin',(0.,0.,0.));
#5420=CARTESIAN_POINT('',(-0.335,0.0149999999999999,-4.10256677714363E-17));
#5421=CARTESIAN_POINT('Origin',(0.22,0.,0.));
#5422=CARTESIAN_POINT('',(-0.22,-6.93889390390723E-18,-2.69422295812418E-17));
#5423=CARTESIAN_POINT('Origin',(0.,0.,0.));
#5424=CARTESIAN_POINT('Origin',(0.,-0.02,0.));
#5425=CARTESIAN_POINT('',(-0.1954,-0.0492,2.39295984553393E-17));
#5426=CARTESIAN_POINT('Origin',(0.,-0.0492,0.));
#5427=CARTESIAN_POINT('',(-0.21,-0.02,-2.57175827820944E-17));
#5428=CARTESIAN_POINT('Origin',(0.,-0.8,0.));
#5429=CARTESIAN_POINT('',(-0.1954,-0.8,-2.39295984553393E-17));
#5683=UNCERTAINTY_MEASURE_WITH_UNIT(LENGTH_MEASURE(0.001),#5703,
'DISTANCE_ACCURACY_VALUE',
'Maximum model space distance between geometric entities at asserted c
onnectivities');
#5688=UNCERTAINTY_MEASURE_WITH_UNIT(LENGTH_MEASURE(0.001),#5703,
'DISTANCE_ACCURACY_VALUE',
'Maximum model space distance between geometric entities at asserted c
onnectivities');
#5697=(
GEOMETRIC_REPRESENTATION_CONTEXT(3)
GLOBAL_UNCERTAINTY_ASSIGNED_CONTEXT((#5683))
GLOBAL_UNIT_ASSIGNED_CONTEXT((#5703,#5705,#5706))
REPRESENTATION_CONTEXT('','3D')
);
#5702=(
GEOMETRIC_REPRESENTATION_CONTEXT(3)
GLOBAL_UNCERTAINTY_ASSIGNED_CONTEXT((#5688))
GLOBAL_UNIT_ASSIGNED_CONTEXT((#5703,#5705,#5706))
REPRESENTATION_CONTEXT('','3D')
);
#5703=(
LENGTH_UNIT()
NAMED_UNIT(*)
SI_UNIT(.CENTI.,.METRE.)
);
#5705=(
NAMED_UNIT(*)
PLANE_ANGLE_UNIT()
SI_UNIT($,.RADIAN.)
);
#5706=(
NAMED_UNIT(*)
SI_UNIT($,.STERADIAN.)
SOLID_ANGLE_UNIT()
);
#5715=SHAPE_DEFINITION_REPRESENTATION(#5728,#5767);
#5728=PRODUCT_DEFINITION_SHAPE('',$,#5781);
#5767=SHAPE_REPRESENTATION('',(#3633),#5697);
#5772=PRODUCT_DEFINITION_CONTEXT('part definition',#5813,'design');
#5781=PRODUCT_DEFINITION('M4x10 Cap Screw','M4x10 Cap Screw',
#5794,#5772);
#5794=PRODUCT_DEFINITION_FORMATION('',$,#5823);
#5813=APPLICATION_CONTEXT(
'Core Data for Automotive Mechanical Design Process');
#5814=PRODUCT_CONTEXT('part definition',#5813,'mechanical');
#5823=PRODUCT('M4x10 Cap Screw','M4x10 Cap Screw',
'M4x10 Cap Screw',(#5814));
#5898=COLOUR_RGB('Black',0.12,0.14,0.17);
#5899=FILL_AREA_STYLE_COLOUR('',#5898);
#5900=FILL_AREA_STYLE('',(#5899));
#5901=SURFACE_STYLE_FILL_AREA(#5900);
#5902=SURFACE_SIDE_STYLE('',(#5901));
#5903=SURFACE_STYLE_USAGE(.BOTH.,#5902);
#5904=PRESENTATION_STYLE_ASSIGNMENT((#5903));
ENDSEC;
END-ISO-10303-21;
